ISO-10303-21;
HEADER;
/* Generated by software containing ST-Developer
 * from STEP Tools, Inc. (www.steptools.com) 
 */

FILE_DESCRIPTION(
/* description */ ('PAT-054'),
/* implementation_level */ '2;1');

FILE_NAME(
/* name */ 'Flat Washer - M5.step',
/* time_stamp */ '2026-10-29T16:38:13-07:00',
/* author */ (''),
/* organization */ (''),
/* preprocessor_version */ 'ST-DEVELOPER v20.2',
/* originating_system */ 'Autodesk Translation Framework v15.17.0.0',
/* authorisation */ '');

FILE_SCHEMA (('AUTOMOTIVE_DESIGN { 1 0 10303 214 3 1 1 }'));
ENDSEC;

DATA;
#10=MECHANICAL_DESIGN_GEOMETRIC_PRESENTATION_REPRESENTATION('',(#935),#33981);
#785=CONICAL_SURFACE('',#14201,0.275,0.785398163397449);
#832=SHAPE_REPRESENTATION_RELATIONSHIP('SRR','None',#34207,#876);
#876=ADVANCED_BREP_SHAPE_REPRESENTATION('',(#994),#33955);
#935=STYLED_ITEM('',(#34524),#994);
#994=MANIFOLD_SOLID_BREP('Body1',#13046);
#1149=FACE_BOUND('',#2747,.T.);
#1150=FACE_BOUND('',#2750,.T.);
#1399=PLANE('',#14206);
#1400=PLANE('',#14210);
#1884=FACE_OUTER_BOUND('',#2744,.T.);
#1885=FACE_OUTER_BOUND('',#2745,.T.);
#1886=FACE_OUTER_BOUND('',#2746,.T.);
#1887=FACE_OUTER_BOUND('',#2748,.T.);
#1888=FACE_OUTER_BOUND('',#2749,.T.);
#2744=EDGE_LOOP('',(#9961,#9962,#9963,#9964));
#2745=EDGE_LOOP('',(#9965,#9966,#9967,#9968));
#2746=EDGE_LOOP('',(#9969));
#2747=EDGE_LOOP('',(#9970));
#2748=EDGE_LOOP('',(#9971,#9972,#9973,#9974));
#2749=EDGE_LOOP('',(#9975));
#2750=EDGE_LOOP('',(#9976));
#3644=LINE('',#20711,#4578);
#3645=LINE('',#20715,#4579);
#3646=LINE('',#20722,#4580);
#4578=VECTOR('',#16585,0.275);
#4579=VECTOR('',#16590,0.265);
#4580=VECTOR('',#16599,0.5);
#5400=CIRCLE('',#14202,0.285);
#5401=CIRCLE('',#14203,0.265);
#5402=CIRCLE('',#14205,0.265);
#5403=CIRCLE('',#14207,0.5);
#5404=CIRCLE('',#14209,0.5);
#6078=VERTEX_POINT('',#20708);
#6079=VERTEX_POINT('',#20710);
#6080=VERTEX_POINT('',#20714);
#6081=VERTEX_POINT('',#20718);
#6082=VERTEX_POINT('',#20721);
#7480=EDGE_CURVE('',#6078,#6078,#5400,.T.);
#7481=EDGE_CURVE('',#6078,#6079,#3644,.T.);
#7482=EDGE_CURVE('',#6079,#6079,#5401,.T.);
#7483=EDGE_CURVE('',#6079,#6080,#3645,.T.);
#7484=EDGE_CURVE('',#6080,#6080,#5402,.T.);
#7485=EDGE_CURVE('',#6081,#6081,#5403,.T.);
#7486=EDGE_CURVE('',#6081,#6082,#3646,.T.);
#7487=EDGE_CURVE('',#6082,#6082,#5404,.T.);
#9961=ORIENTED_EDGE('',*,*,#7480,.T.);
#9962=ORIENTED_EDGE('',*,*,#7481,.T.);
#9963=ORIENTED_EDGE('',*,*,#7482,.T.);
#9964=ORIENTED_EDGE('',*,*,#7481,.F.);
#9965=ORIENTED_EDGE('',*,*,#7482,.F.);
#9966=ORIENTED_EDGE('',*,*,#7483,.T.);
#9967=ORIENTED_EDGE('',*,*,#7484,.T.);
#9968=ORIENTED_EDGE('',*,*,#7483,.F.);
#9969=ORIENTED_EDGE('',*,*,#7485,.T.);
#9970=ORIENTED_EDGE('',*,*,#7480,.F.);
#9971=ORIENTED_EDGE('',*,*,#7485,.F.);
#9972=ORIENTED_EDGE('',*,*,#7486,.T.);
#9973=ORIENTED_EDGE('',*,*,#7487,.T.);
#9974=ORIENTED_EDGE('',*,*,#7486,.F.);
#9975=ORIENTED_EDGE('',*,*,#7487,.F.);
#9976=ORIENTED_EDGE('',*,*,#7484,.F.);
#12075=CYLINDRICAL_SURFACE('',#14204,0.265);
#12076=CYLINDRICAL_SURFACE('',#14208,0.5);
#12596=ADVANCED_FACE('',(#1884),#785,.F.);
#12597=ADVANCED_FACE('',(#1885),#12075,.F.);
#12598=ADVANCED_FACE('',(#1886,#1149),#1399,.T.);
#12599=ADVANCED_FACE('',(#1887),#12076,.T.);
#12600=ADVANCED_FACE('',(#1888,#1150),#1400,.F.);
#13046=CLOSED_SHELL('',(#12596,#12597,#12598,#12599,#12600));
#14200=AXIS2_PLACEMENT_3D('',#20706,#16579,#16580);
#14201=AXIS2_PLACEMENT_3D('',#20707,#16581,#16582);
#14202=AXIS2_PLACEMENT_3D('',#20709,#16583,#16584);
#14203=AXIS2_PLACEMENT_3D('',#20712,#16586,#16587);
#14204=AXIS2_PLACEMENT_3D('',#20713,#16588,#16589);
#14205=AXIS2_PLACEMENT_3D('',#20716,#16591,#16592);
#14206=AXIS2_PLACEMENT_3D('',#20717,#16593,#16594);
#14207=AXIS2_PLACEMENT_3D('',#20719,#16595,#16596);
#14208=AXIS2_PLACEMENT_3D('',#20720,#16597,#16598);
#14209=AXIS2_PLACEMENT_3D('',#20723,#16600,#16601);
#14210=AXIS2_PLACEMENT_3D('',#20724,#16602,#16603);
#16579=DIRECTION('axis',(0.,0.,1.));
#16580=DIRECTION('refdir',(1.,0.,0.));
#16581=DIRECTION('center_axis',(0.,1.,0.));
#16582=DIRECTION('ref_axis',(1.,0.,0.));
#16583=DIRECTION('center_axis',(0.,1.,0.));
#16584=DIRECTION('ref_axis',(1.,0.,0.));
#16585=DIRECTION('',(0.707106781186548,-0.707106781186547,-8.65956056235494E-17));
#16586=DIRECTION('center_axis',(0.,-1.,0.));
#16587=DIRECTION('ref_axis',(1.,0.,0.));
#16588=DIRECTION('center_axis',(0.,1.,0.));
#16589=DIRECTION('ref_axis',(1.,0.,0.));
#16590=DIRECTION('',(0.,-1.,0.));
#16591=DIRECTION('center_axis',(0.,-1.,0.));
#16592=DIRECTION('ref_axis',(1.,0.,0.));
#16593=DIRECTION('center_axis',(0.,1.,0.));
#16594=DIRECTION('ref_axis',(1.,0.,0.));
#16595=DIRECTION('center_axis',(0.,1.,0.));
#16596=DIRECTION('ref_axis',(1.,0.,0.));
#16597=DIRECTION('center_axis',(0.,1.,0.));
#16598=DIRECTION('ref_axis',(1.,0.,0.));
#16599=DIRECTION('',(0.,-1.,0.));
#16600=DIRECTION('center_axis',(0.,1.,0.));
#16601=DIRECTION('ref_axis',(1.,0.,0.));
#16602=DIRECTION('center_axis',(0.,1.,0.));
#16603=DIRECTION('ref_axis',(1.,0.,0.));
#20706=CARTESIAN_POINT('',(0.,0.,0.));
#20707=CARTESIAN_POINT('Origin',(0.,0.09,0.));
#20708=CARTESIAN_POINT('',(-0.285,0.1,3.49024337756996E-17));
#20709=CARTESIAN_POINT('Origin',(0.,0.1,0.));
#20710=CARTESIAN_POINT('',(-0.265,0.08,-3.24531401774049E-17));
#20711=CARTESIAN_POINT('',(-0.275,0.09,3.36777869765522E-17));
#20712=CARTESIAN_POINT('Origin',(0.,0.08,0.));
#20713=CARTESIAN_POINT('Origin',(0.,0.,0.));
#20714=CARTESIAN_POINT('',(-0.265,0.,3.24531401774049E-17));
#20715=CARTESIAN_POINT('',(-0.265,0.,3.24531401774049E-17));
#20716=CARTESIAN_POINT('Origin',(0.,0.,0.));
#20717=CARTESIAN_POINT('Origin',(0.,0.1,0.));
#20718=CARTESIAN_POINT('',(-0.5,0.1,6.12323399573677E-17));
#20719=CARTESIAN_POINT('Origin',(0.,0.1,0.));
#20720=CARTESIAN_POINT('Origin',(0.,0.,0.));
#20721=CARTESIAN_POINT('',(-0.5,0.,6.12323399573677E-17));
#20722=CARTESIAN_POINT('',(-0.5,0.,6.12323399573677E-17));
#20723=CARTESIAN_POINT('Origin',(0.,0.,0.));
#20724=CARTESIAN_POINT('Origin',(0.,0.,0.));
#33903=UNCERTAINTY_MEASURE_WITH_UNIT(LENGTH_MEASURE(0.001),#33982,
'DISTANCE_ACCURACY_VALUE',
'Maximum model space distance between geometric entities at asserted c
onnectivities');
#33929=UNCERTAINTY_MEASURE_WITH_UNIT(LENGTH_MEASURE(0.001),#33982,
'DISTANCE_ACCURACY_VALUE',
'Maximum model space distance between geometric entities at asserted c
onnectivities');
#33955=(
GEOMETRIC_REPRESENTATION_CONTEXT(3)
GLOBAL_UNCERTAINTY_ASSIGNED_CONTEXT((#33903))
GLOBAL_UNIT_ASSIGNED_CONTEXT((#33982,#33984,#33985))
REPRESENTATION_CONTEXT('','3D')
);
#33981=(
GEOMETRIC_REPRESENTATION_CONTEXT(3)
GLOBAL_UNCERTAINTY_ASSIGNED_CONTEXT((#33929))
GLOBAL_UNIT_ASSIGNED_CONTEXT((#33982,#33984,#33985))
REPRESENTATION_CONTEXT('','3D')
);
#33982=(
LENGTH_UNIT()
NAMED_UNIT(*)
SI_UNIT(.CENTI.,.METRE.)
);
#33984=(
NAMED_UNIT(*)
PLANE_ANGLE_UNIT()
SI_UNIT($,.RADIAN.)
);
#33985=(
NAMED_UNIT(*)
SI_UNIT($,.STERADIAN.)
SOLID_ANGLE_UNIT()
);
#34011=SHAPE_DEFINITION_REPRESENTATION(#34072,#34207);
#34072=PRODUCT_DEFINITION_SHAPE('',$,#34259);
#34207=SHAPE_REPRESENTATION('',(#14200),#33955);
#34233=PRODUCT_DEFINITION_CONTEXT('part definition',#34388,'design');
#34259=PRODUCT_DEFINITION('Flat Washer - M5','Flat Washer - M5',#34310,
#34233);
#34310=PRODUCT_DEFINITION_FORMATION('',$,#34415);
#34388=APPLICATION_CONTEXT(
'Core Data for Automotive Mechanical Design Process');
#34389=PRODUCT_CONTEXT('part definition',#34388,'mechanical');
#34415=PRODUCT('Flat Washer - M5','Flat Washer - M5','Flat Washer - M5',
(#34389));
#34518=COLOUR_RGB('Black',0.12,0.14,0.17);
#34519=FILL_AREA_STYLE_COLOUR('',#34518);
#34520=FILL_AREA_STYLE('',(#34519));
#34521=SURFACE_STYLE_FILL_AREA(#34520);
#34522=SURFACE_SIDE_STYLE('',(#34521));
#34523=SURFACE_STYLE_USAGE(.BOTH.,#34522);
#34524=PRESENTATION_STYLE_ASSIGNMENT((#34523));
ENDSEC;
END-ISO-10303-21;
